ISO-10303-21;
HEADER;
/* Generated by software containing ST-Developer
 * from STEP Tools, Inc. (www.steptools.com) 
 */

FILE_DESCRIPTION(
/* description */ ('Cam-and-follower valve demonstrator'),
/* implementation_level */ '2;1');

FILE_NAME(
/* name */ 'Bearing cap (1).step',
/* time_stamp */ '2026-10-28T03:25:17-07:00',
/* author */ (''),
/* organization */ (''),
/* preprocessor_version */ 'ST-DEVELOPER v20.2',
/* originating_system */ 'Autodesk Translation Framework v15.17.0.0',
/* authorisation */ '');

FILE_SCHEMA (('AUTOMOTIVE_DESIGN { 1 0 10303 214 3 1 1 }'));
ENDSEC;

DATA;
#10=MECHANICAL_DESIGN_GEOMETRIC_PRESENTATION_REPRESENTATION('',(#417),#12896);
#345=SHAPE_REPRESENTATION_RELATIONSHIP('SRR','None',#13061,#381);
#381=ADVANCED_BREP_SHAPE_REPRESENTATION('',(#460),#12861);
#417=STYLED_ITEM('',(#13330),#460);
#460=MANIFOLD_SOLID_BREP('Body1',#6184);
#533=FACE_BOUND('',#1563,.T.);
#534=FACE_BOUND('',#1567,.T.);
#535=FACE_BOUND('',#1568,.T.);
#536=FACE_BOUND('',#1569,.T.);
#537=FACE_BOUND('',#1570,.T.);
#538=FACE_BOUND('',#1571,.T.);
#539=FACE_BOUND('',#1573,.T.);
#540=FACE_BOUND('',#1574,.T.);
#541=FACE_BOUND('',#1575,.T.);
#542=FACE_BOUND('',#1576,.T.);
#543=FACE_BOUND('',#1577,.T.);
#699=CIRCLE('',#6727,0.225);
#700=CIRCLE('',#6728,0.225);
#701=CIRCLE('',#6730,0.225);
#702=CIRCLE('',#6731,0.225);
#703=CIRCLE('',#6733,0.225);
#704=CIRCLE('',#6734,0.225);
#705=CIRCLE('',#6736,0.225);
#706=CIRCLE('',#6737,0.225);
#707=CIRCLE('',#6739,1.59);
#708=CIRCLE('',#6740,1.59);
#709=CIRCLE('',#6742,1.005);
#710=CIRCLE('',#6744,1.005);
#711=CIRCLE('',#6746,2.4);
#712=CIRCLE('',#6747,2.4);
#993=CYLINDRICAL_SURFACE('',#6726,0.225);
#994=CYLINDRICAL_SURFACE('',#6729,0.225);
#995=CYLINDRICAL_SURFACE('',#6732,0.225);
#996=CYLINDRICAL_SURFACE('',#6735,0.225);
#997=CYLINDRICAL_SURFACE('',#6738,1.59);
#998=CYLINDRICAL_SURFACE('',#6743,1.005);
#999=CYLINDRICAL_SURFACE('',#6745,2.4);
#1151=FACE_OUTER_BOUND('',#1557,.T.);
#1152=FACE_OUTER_BOUND('',#1558,.T.);
#1153=FACE_OUTER_BOUND('',#1559,.T.);
#1154=FACE_OUTER_BOUND('',#1560,.T.);
#1155=FACE_OUTER_BOUND('',#1561,.T.);
#1156=FACE_OUTER_BOUND('',#1562,.T.);
#1157=FACE_OUTER_BOUND('',#1564,.T.);
#1158=FACE_OUTER_BOUND('',#1565,.T.);
#1159=FACE_OUTER_BOUND('',#1566,.T.);
#1160=FACE_OUTER_BOUND('',#1572,.T.);
#1557=EDGE_LOOP('',(#4359,#4360,#4361,#4362));
#1558=EDGE_LOOP('',(#4363,#4364,#4365,#4366));
#1559=EDGE_LOOP('',(#4367,#4368,#4369,#4370));
#1560=EDGE_LOOP('',(#4371,#4372,#4373,#4374));
#1561=EDGE_LOOP('',(#4375,#4376,#4377,#4378));
#1562=EDGE_LOOP('',(#4379));
#1563=EDGE_LOOP('',(#4380));
#1564=EDGE_LOOP('',(#4381,#4382,#4383,#4384));
#1565=EDGE_LOOP('',(#4385,#4386,#4387,#4388));
#1566=EDGE_LOOP('',(#4389));
#1567=EDGE_LOOP('',(#4390));
#1568=EDGE_LOOP('',(#4391));
#1569=EDGE_LOOP('',(#4392));
#1570=EDGE_LOOP('',(#4393));
#1571=EDGE_LOOP('',(#4394));
#1572=EDGE_LOOP('',(#4395));
#1573=EDGE_LOOP('',(#4396));
#1574=EDGE_LOOP('',(#4397));
#1575=EDGE_LOOP('',(#4398));
#1576=EDGE_LOOP('',(#4399));
#1577=EDGE_LOOP('',(#4400));
#2087=LINE('',#9708,#2509);
#2088=LINE('',#9714,#2510);
#2089=LINE('',#9720,#2511);
#2090=LINE('',#9726,#2512);
#2091=LINE('',#9732,#2513);
#2092=LINE('',#9740,#2514);
#2093=LINE('',#9745,#2515);
#2509=VECTOR('',#7718,0.225);
#2510=VECTOR('',#7725,0.225);
#2511=VECTOR('',#7732,0.225);
#2512=VECTOR('',#7739,0.225);
#2513=VECTOR('',#7746,1.59);
#2514=VECTOR('',#7757,1.005);
#2515=VECTOR('',#7762,2.4);
#2927=VERTEX_POINT('',#9705);
#2928=VERTEX_POINT('',#9707);
#2929=VERTEX_POINT('',#9711);
#2930=VERTEX_POINT('',#9713);
#2931=VERTEX_POINT('',#9717);
#2932=VERTEX_POINT('',#9719);
#2933=VERTEX_POINT('',#9723);
#2934=VERTEX_POINT('',#9725);
#2935=VERTEX_POINT('',#9729);
#2936=VERTEX_POINT('',#9731);
#2937=VERTEX_POINT('',#9735);
#2938=VERTEX_POINT('',#9738);
#2939=VERTEX_POINT('',#9742);
#2940=VERTEX_POINT('',#9744);
#3476=EDGE_CURVE('',#2927,#2927,#699,.T.);
#3477=EDGE_CURVE('',#2927,#2928,#2087,.T.);
#3478=EDGE_CURVE('',#2928,#2928,#700,.T.);
#3479=EDGE_CURVE('',#2929,#2929,#701,.T.);
#3480=EDGE_CURVE('',#2929,#2930,#2088,.T.);
#3481=EDGE_CURVE('',#2930,#2930,#702,.T.);
#3482=EDGE_CURVE('',#2931,#2931,#703,.T.);
#3483=EDGE_CURVE('',#2931,#2932,#2089,.T.);
#3484=EDGE_CURVE('',#2932,#2932,#704,.T.);
#3485=EDGE_CURVE('',#2933,#2933,#705,.T.);
#3486=EDGE_CURVE('',#2933,#2934,#2090,.T.);
#3487=EDGE_CURVE('',#2934,#2934,#706,.T.);
#3488=EDGE_CURVE('',#2935,#2935,#707,.T.);
#3489=EDGE_CURVE('',#2935,#2936,#2091,.T.);
#3490=EDGE_CURVE('',#2936,#2936,#708,.T.);
#3491=EDGE_CURVE('',#2937,#2937,#709,.T.);
#3492=EDGE_CURVE('',#2938,#2938,#710,.T.);
#3493=EDGE_CURVE('',#2938,#2937,#2092,.T.);
#3494=EDGE_CURVE('',#2939,#2939,#711,.T.);
#3495=EDGE_CURVE('',#2939,#2940,#2093,.T.);
#3496=EDGE_CURVE('',#2940,#2940,#712,.T.);
#4359=ORIENTED_EDGE('',*,*,#3476,.F.);
#4360=ORIENTED_EDGE('',*,*,#3477,.T.);
#4361=ORIENTED_EDGE('',*,*,#3478,.F.);
#4362=ORIENTED_EDGE('',*,*,#3477,.F.);
#4363=ORIENTED_EDGE('',*,*,#3479,.F.);
#4364=ORIENTED_EDGE('',*,*,#3480,.T.);
#4365=ORIENTED_EDGE('',*,*,#3481,.F.);
#4366=ORIENTED_EDGE('',*,*,#3480,.F.);
#4367=ORIENTED_EDGE('',*,*,#3482,.F.);
#4368=ORIENTED_EDGE('',*,*,#3483,.T.);
#4369=ORIENTED_EDGE('',*,*,#3484,.F.);
#4370=ORIENTED_EDGE('',*,*,#3483,.F.);
#4371=ORIENTED_EDGE('',*,*,#3485,.F.);
#4372=ORIENTED_EDGE('',*,*,#3486,.T.);
#4373=ORIENTED_EDGE('',*,*,#3487,.F.);
#4374=ORIENTED_EDGE('',*,*,#3486,.F.);
#4375=ORIENTED_EDGE('',*,*,#3488,.F.);
#4376=ORIENTED_EDGE('',*,*,#3489,.T.);
#4377=ORIENTED_EDGE('',*,*,#3490,.T.);
#4378=ORIENTED_EDGE('',*,*,#3489,.F.);
#4379=ORIENTED_EDGE('',*,*,#3490,.F.);
#4380=ORIENTED_EDGE('',*,*,#3491,.F.);
#4381=ORIENTED_EDGE('',*,*,#3492,.F.);
#4382=ORIENTED_EDGE('',*,*,#3493,.T.);
#4383=ORIENTED_EDGE('',*,*,#3491,.T.);
#4384=ORIENTED_EDGE('',*,*,#3493,.F.);
#4385=ORIENTED_EDGE('',*,*,#3494,.F.);
#4386=ORIENTED_EDGE('',*,*,#3495,.T.);
#4387=ORIENTED_EDGE('',*,*,#3496,.T.);
#4388=ORIENTED_EDGE('',*,*,#3495,.F.);
#4389=ORIENTED_EDGE('',*,*,#3494,.T.);
#4390=ORIENTED_EDGE('',*,*,#3492,.T.);
#4391=ORIENTED_EDGE('',*,*,#3487,.T.);
#4392=ORIENTED_EDGE('',*,*,#3484,.T.);
#4393=ORIENTED_EDGE('',*,*,#3481,.T.);
#4394=ORIENTED_EDGE('',*,*,#3478,.T.);
#4395=ORIENTED_EDGE('',*,*,#3496,.F.);
#4396=ORIENTED_EDGE('',*,*,#3488,.T.);
#4397=ORIENTED_EDGE('',*,*,#3485,.T.);
#4398=ORIENTED_EDGE('',*,*,#3482,.T.);
#4399=ORIENTED_EDGE('',*,*,#3479,.T.);
#4400=ORIENTED_EDGE('',*,*,#3476,.T.);
#5633=PLANE('',#6741);
#5634=PLANE('',#6748);
#5635=PLANE('',#6749);
#5867=ADVANCED_FACE('',(#1151),#993,.F.);
#5868=ADVANCED_FACE('',(#1152),#994,.F.);
#5869=ADVANCED_FACE('',(#1153),#995,.F.);
#5870=ADVANCED_FACE('',(#1154),#996,.F.);
#5871=ADVANCED_FACE('',(#1155),#997,.T.);
#5872=ADVANCED_FACE('',(#1156,#533),#5633,.F.);
#5873=ADVANCED_FACE('',(#1157),#998,.F.);
#5874=ADVANCED_FACE('',(#1158),#999,.T.);
#5875=ADVANCED_FACE('',(#1159,#534,#535,#536,#537,#538),#5634,.T.);
#5876=ADVANCED_FACE('',(#1160,#539,#540,#541,#542,#543),#5635,.F.);
#6184=CLOSED_SHELL('',(#5867,#5868,#5869,#5870,#5871,#5872,#5873,#5874,
#5875,#5876));
#6725=AXIS2_PLACEMENT_3D('',#9703,#7712,#7713);
#6726=AXIS2_PLACEMENT_3D('',#9704,#7714,#7715);
#6727=AXIS2_PLACEMENT_3D('',#9706,#7716,#7717);
#6728=AXIS2_PLACEMENT_3D('',#9709,#7719,#7720);
#6729=AXIS2_PLACEMENT_3D('',#9710,#7721,#7722);
#6730=AXIS2_PLACEMENT_3D('',#9712,#7723,#7724);
#6731=AXIS2_PLACEMENT_3D('',#9715,#7726,#7727);
#6732=AXIS2_PLACEMENT_3D('',#9716,#7728,#7729);
#6733=AXIS2_PLACEMENT_3D('',#9718,#7730,#7731);
#6734=AXIS2_PLACEMENT_3D('',#9721,#7733,#7734);
#6735=AXIS2_PLACEMENT_3D('',#9722,#7735,#7736);
#6736=AXIS2_PLACEMENT_3D('',#9724,#7737,#7738);
#6737=AXIS2_PLACEMENT_3D('',#9727,#7740,#7741);
#6738=AXIS2_PLACEMENT_3D('',#9728,#7742,#7743);
#6739=AXIS2_PLACEMENT_3D('',#9730,#7744,#7745);
#6740=AXIS2_PLACEMENT_3D('',#9733,#7747,#7748);
#6741=AXIS2_PLACEMENT_3D('',#9734,#7749,#7750);
#6742=AXIS2_PLACEMENT_3D('',#9736,#7751,#7752);
#6743=AXIS2_PLACEMENT_3D('',#9737,#7753,#7754);
#6744=AXIS2_PLACEMENT_3D('',#9739,#7755,#7756);
#6745=AXIS2_PLACEMENT_3D('',#9741,#7758,#7759);
#6746=AXIS2_PLACEMENT_3D('',#9743,#7760,#7761);
#6747=AXIS2_PLACEMENT_3D('',#9746,#7763,#7764);
#6748=AXIS2_PLACEMENT_3D('',#9747,#7765,#7766);
#6749=AXIS2_PLACEMENT_3D('',#9748,#7767,#7768);
#7712=DIRECTION('axis',(0.,0.,1.));
#7713=DIRECTION('refdir',(1.,0.,0.));
#7714=DIRECTION('center_axis',(0.,1.,0.));
#7715=DIRECTION('ref_axis',(1.,0.,0.));
#7716=DIRECTION('center_axis',(0.,1.,0.));
#7717=DIRECTION('ref_axis',(1.,0.,0.));
#7718=DIRECTION('',(0.,1.,0.));
#7719=DIRECTION('center_axis',(0.,-1.,0.));
#7720=DIRECTION('ref_axis',(1.,0.,0.));
#7721=DIRECTION('center_axis',(0.,1.,0.));
#7722=DIRECTION('ref_axis',(1.,0.,0.));
#7723=DIRECTION('center_axis',(0.,1.,0.));
#7724=DIRECTION('ref_axis',(1.,0.,0.));
#7725=DIRECTION('',(0.,1.,0.));
#7726=DIRECTION('center_axis',(0.,-1.,0.));
#7727=DIRECTION('ref_axis',(1.,0.,0.));
#7728=DIRECTION('center_axis',(0.,1.,0.));
#7729=DIRECTION('ref_axis',(1.,0.,0.));
#7730=DIRECTION('center_axis',(0.,1.,0.));
#7731=DIRECTION('ref_axis',(1.,0.,0.));
#7732=DIRECTION('',(0.,1.,0.));
#7733=DIRECTION('center_axis',(0.,-1.,0.));
#7734=DIRECTION('ref_axis',(1.,0.,0.));
#7735=DIRECTION('center_axis',(0.,1.,0.));
#7736=DIRECTION('ref_axis',(1.,0.,0.));
#7737=DIRECTION('center_axis',(0.,1.,0.));
#7738=DIRECTION('ref_axis',(1.,0.,0.));
#7739=DIRECTION('',(0.,1.,0.));
#7740=DIRECTION('center_axis',(0.,-1.,0.));
#7741=DIRECTION('ref_axis',(1.,0.,0.));
#7742=DIRECTION('center_axis',(0.,1.,0.));
#7743=DIRECTION('ref_axis',(1.,0.,0.));
#7744=DIRECTION('center_axis',(0.,1.,0.));
#7745=DIRECTION('ref_axis',(1.,0.,0.));
#7746=DIRECTION('',(0.,-1.,0.));
#7747=DIRECTION('center_axis',(0.,1.,0.));
#7748=DIRECTION('ref_axis',(1.,0.,0.));
#7749=DIRECTION('center_axis',(0.,1.,0.));
#7750=DIRECTION('ref_axis',(1.,0.,0.));
#7751=DIRECTION('center_axis',(0.,-1.,0.));
#7752=DIRECTION('ref_axis',(1.,0.,0.));
#7753=DIRECTION('center_axis',(0.,1.,0.));
#7754=DIRECTION('ref_axis',(1.,0.,0.));
#7755=DIRECTION('center_axis',(0.,-1.,0.));
#7756=DIRECTION('ref_axis',(1.,0.,0.));
#7757=DIRECTION('',(0.,-1.,0.));
#7758=DIRECTION('center_axis',(0.,1.,0.));
#7759=DIRECTION('ref_axis',(1.,0.,0.));
#7760=DIRECTION('center_axis',(0.,1.,0.));
#7761=DIRECTION('ref_axis',(1.,0.,0.));
#7762=DIRECTION('',(0.,-1.,0.));
#7763=DIRECTION('center_axis',(0.,1.,0.));
#7764=DIRECTION('ref_axis',(1.,0.,0.));
#7765=DIRECTION('center_axis',(0.,1.,0.));
#7766=DIRECTION('ref_axis',(1.,0.,0.));
#7767=DIRECTION('center_axis',(0.,1.,0.));
#7768=DIRECTION('ref_axis',(1.,0.,0.));
#9703=CARTESIAN_POINT('',(0.,0.,0.));
#9704=CARTESIAN_POINT('Origin',(-1.4142135623731,-1.8,2.58578643762691));
#9705=CARTESIAN_POINT('',(-1.6392135623731,-1.7,2.58578643762691));
#9706=CARTESIAN_POINT('Origin',(-1.4142135623731,-1.7,2.58578643762691));
#9707=CARTESIAN_POINT('',(-1.6392135623731,-1.5,2.58578643762691));
#9708=CARTESIAN_POINT('',(-1.6392135623731,-1.8,2.58578643762691));
#9709=CARTESIAN_POINT('Origin',(-1.4142135623731,-1.5,2.58578643762691));
#9710=CARTESIAN_POINT('Origin',(-1.41421356237309,-1.8,5.41421356237309));
#9711=CARTESIAN_POINT('',(-1.6392135623731,-1.7,5.41421356237309));
#9712=CARTESIAN_POINT('Origin',(-1.41421356237309,-1.7,5.41421356237309));
#9713=CARTESIAN_POINT('',(-1.6392135623731,-1.5,5.41421356237309));
#9714=CARTESIAN_POINT('',(-1.6392135623731,-1.8,5.41421356237309));
#9715=CARTESIAN_POINT('Origin',(-1.41421356237309,-1.5,5.41421356237309));
#9716=CARTESIAN_POINT('Origin',(1.4142135623731,-1.8,5.41421356237309));
#9717=CARTESIAN_POINT('',(1.1892135623731,-1.7,5.41421356237309));
#9718=CARTESIAN_POINT('Origin',(1.4142135623731,-1.7,5.41421356237309));
#9719=CARTESIAN_POINT('',(1.1892135623731,-1.5,5.41421356237309));
#9720=CARTESIAN_POINT('',(1.1892135623731,-1.8,5.41421356237309));
#9721=CARTESIAN_POINT('Origin',(1.4142135623731,-1.5,5.41421356237309));
#9722=CARTESIAN_POINT('Origin',(1.41421356237309,-1.8,2.5857864376269));
#9723=CARTESIAN_POINT('',(1.18921356237309,-1.7,2.5857864376269));
#9724=CARTESIAN_POINT('Origin',(1.41421356237309,-1.7,2.5857864376269));
#9725=CARTESIAN_POINT('',(1.18921356237309,-1.5,2.5857864376269));
#9726=CARTESIAN_POINT('',(1.18921356237309,-1.8,2.5857864376269));
#9727=CARTESIAN_POINT('Origin',(1.41421356237309,-1.5,2.5857864376269));
#9728=CARTESIAN_POINT('Origin',(0.,-2.,4.));
#9729=CARTESIAN_POINT('',(-1.59,-1.7,4.));
#9730=CARTESIAN_POINT('Origin',(0.,-1.7,4.));
#9731=CARTESIAN_POINT('',(-1.59,-2.,4.));
#9732=CARTESIAN_POINT('',(-1.59,-2.,4.));
#9733=CARTESIAN_POINT('Origin',(0.,-2.,4.));
#9734=CARTESIAN_POINT('Origin',(0.,-2.,4.));
#9735=CARTESIAN_POINT('',(-1.005,-2.,4.));
#9736=CARTESIAN_POINT('Origin',(0.,-2.,4.));
#9737=CARTESIAN_POINT('Origin',(0.,-1.7,4.));
#9738=CARTESIAN_POINT('',(-1.005,-1.5,4.));
#9739=CARTESIAN_POINT('Origin',(0.,-1.5,4.));
#9740=CARTESIAN_POINT('',(-1.005,-1.7,4.));
#9741=CARTESIAN_POINT('Origin',(0.,-1.7,4.));
#9742=CARTESIAN_POINT('',(-2.4,-1.5,4.));
#9743=CARTESIAN_POINT('Origin',(0.,-1.5,4.));
#9744=CARTESIAN_POINT('',(-2.4,-1.7,4.));
#9745=CARTESIAN_POINT('',(-2.4,-1.7,4.));
#9746=CARTESIAN_POINT('Origin',(0.,-1.7,4.));
#9747=CARTESIAN_POINT('Origin',(0.,-1.5,4.));
#9748=CARTESIAN_POINT('Origin',(0.,-1.7,4.));
#12818=UNCERTAINTY_MEASURE_WITH_UNIT(LENGTH_MEASURE(0.001),#12897,
'DISTANCE_ACCURACY_VALUE',
'Maximum model space distance between geometric entities at asserted c
onnectivities');
#12853=UNCERTAINTY_MEASURE_WITH_UNIT(LENGTH_MEASURE(0.001),#12897,
'DISTANCE_ACCURACY_VALUE',
'Maximum model space distance between geometric entities at asserted c
onnectivities');
#12861=(
GEOMETRIC_REPRESENTATION_CONTEXT(3)
GLOBAL_UNCERTAINTY_ASSIGNED_CONTEXT((#12818))
GLOBAL_UNIT_ASSIGNED_CONTEXT((#12897,#12899,#12900))
REPRESENTATION_CONTEXT('','3D')
);
#12896=(
GEOMETRIC_REPRESENTATION_CONTEXT(3)
GLOBAL_UNCERTAINTY_ASSIGNED_CONTEXT((#12853))
GLOBAL_UNIT_ASSIGNED_CONTEXT((#12897,#12899,#12900))
REPRESENTATION_CONTEXT('','3D')
);
#12897=(
LENGTH_UNIT()
NAMED_UNIT(*)
SI_UNIT(.CENTI.,.METRE.)
);
#12899=(
NAMED_UNIT(*)
PLANE_ANGLE_UNIT()
SI_UNIT($,.RADIAN.)
);
#12900=(
NAMED_UNIT(*)
SI_UNIT($,.STERADIAN.)
SOLID_ANGLE_UNIT()
);
#12908=SHAPE_DEFINITION_REPRESENTATION(#12950,#13061);
#12950=PRODUCT_DEFINITION_SHAPE('',$,#13104);
#13061=SHAPE_REPRESENTATION('',(#6725),#12861);
#13096=PRODUCT_DEFINITION_CONTEXT('part definition',#13224,'design');
#13104=PRODUCT_DEFINITION('Bearing cap (1)','Bearing cap (1)',#13146,#13096);
#13146=PRODUCT_DEFINITION_FORMATION('',$,#13233);
#13224=APPLICATION_CONTEXT(
'Core Data for Automotive Mechanical Design Process');
#13225=PRODUCT_CONTEXT('part definition',#13224,'mechanical');
#13233=PRODUCT('Bearing cap (1)','Bearing cap (1)','Bearing cap (1)',(#13225));
#13324=COLOUR_RGB('Grey',0.48,0.52,0.57);
#13325=FILL_AREA_STYLE_COLOUR('',#13324);
#13326=FILL_AREA_STYLE('',(#13325));
#13327=SURFACE_STYLE_FILL_AREA(#13326);
#13328=SURFACE_SIDE_STYLE('',(#13327));
#13329=SURFACE_STYLE_USAGE(.BOTH.,#13328);
#13330=PRESENTATION_STYLE_ASSIGNMENT((#13329));
ENDSEC;
END-ISO-10303-21;
